ISO-10303-21;
HEADER;
/* Generated by software containing ST-Developer
 * from STEP Tools, Inc. (www.steptools.com) 
 */

FILE_DESCRIPTION(
/* description */ ('Turntable on roller ring'),
/* implementation_level */ '2;1');

FILE_NAME(
/* name */ 'Outer race retainer (4).step',
/* time_stamp */ '2026-10-28T03:23:59-07:00',
/* author */ (''),
/* organization */ (''),
/* preprocessor_version */ 'ST-DEVELOPER v20.2',
/* originating_system */ 'Autodesk Translation Framework v15.17.0.0',
/* authorisation */ '');

FILE_SCHEMA (('AUTOMOTIVE_DESIGN { 1 0 10303 214 3 1 1 }'));
ENDSEC;

DATA;
#10=MECHANICAL_DESIGN_GEOMETRIC_PRESENTATION_REPRESENTATION('',(#671),#16281);
#552=SHAPE_REPRESENTATION_RELATIONSHIP('SRR','None',#16575,#607);
#607=ADVANCED_BREP_SHAPE_REPRESENTATION('',(#739),#16269);
#671=STYLED_ITEM('',(#16932),#739);
#739=MANIFOLD_SOLID_BREP('Body1',#8416);
#971=FACE_BOUND('',#2406,.T.);
#972=FACE_BOUND('',#2408,.T.);
#1223=PLANE('',#10001);
#1224=PLANE('',#10002);
#1684=FACE_OUTER_BOUND('',#2403,.T.);
#1685=FACE_OUTER_BOUND('',#2404,.T.);
#1686=FACE_OUTER_BOUND('',#2405,.T.);
#1687=FACE_OUTER_BOUND('',#2407,.T.);
#2403=EDGE_LOOP('',(#7397,#7398,#7399,#7400));
#2404=EDGE_LOOP('',(#7401,#7402,#7403,#7404));
#2405=EDGE_LOOP('',(#7405));
#2406=EDGE_LOOP('',(#7406));
#2407=EDGE_LOOP('',(#7407));
#2408=EDGE_LOOP('',(#7408));
#2950=LINE('',#15461,#3433);
#2951=LINE('',#15467,#3434);
#3433=VECTOR('',#12571,1.1);
#3434=VECTOR('',#12578,1.5);
#3857=CIRCLE('',#9996,1.1);
#3858=CIRCLE('',#9997,1.1);
#3859=CIRCLE('',#9999,1.5);
#3860=CIRCLE('',#10000,1.5);
#4533=VERTEX_POINT('',#15458);
#4534=VERTEX_POINT('',#15460);
#4535=VERTEX_POINT('',#15464);
#4536=VERTEX_POINT('',#15466);
#5509=EDGE_CURVE('',#4533,#4533,#3857,.T.);
#5510=EDGE_CURVE('',#4533,#4534,#2950,.T.);
#5511=EDGE_CURVE('',#4534,#4534,#3858,.T.);
#5512=EDGE_CURVE('',#4535,#4535,#3859,.T.);
#5513=EDGE_CURVE('',#4535,#4536,#2951,.T.);
#5514=EDGE_CURVE('',#4536,#4536,#3860,.T.);
#7397=ORIENTED_EDGE('',*,*,#5509,.F.);
#7398=ORIENTED_EDGE('',*,*,#5510,.T.);
#7399=ORIENTED_EDGE('',*,*,#5511,.T.);
#7400=ORIENTED_EDGE('',*,*,#5510,.F.);
#7401=ORIENTED_EDGE('',*,*,#5512,.F.);
#7402=ORIENTED_EDGE('',*,*,#5513,.T.);
#7403=ORIENTED_EDGE('',*,*,#5514,.T.);
#7404=ORIENTED_EDGE('',*,*,#5513,.F.);
#7405=ORIENTED_EDGE('',*,*,#5512,.T.);
#7406=ORIENTED_EDGE('',*,*,#5509,.T.);
#7407=ORIENTED_EDGE('',*,*,#5514,.F.);
#7408=ORIENTED_EDGE('',*,*,#5511,.F.);
#7831=CYLINDRICAL_SURFACE('',#9995,1.1);
#7832=CYLINDRICAL_SURFACE('',#9998,1.5);
#8287=ADVANCED_FACE('',(#1684),#7831,.F.);
#8288=ADVANCED_FACE('',(#1685),#7832,.T.);
#8289=ADVANCED_FACE('',(#1686,#971),#1223,.T.);
#8290=ADVANCED_FACE('',(#1687,#972),#1224,.F.);
#8416=CLOSED_SHELL('',(#8287,#8288,#8289,#8290));
#9994=AXIS2_PLACEMENT_3D('',#15456,#12565,#12566);
#9995=AXIS2_PLACEMENT_3D('',#15457,#12567,#12568);
#9996=AXIS2_PLACEMENT_3D('',#15459,#12569,#12570);
#9997=AXIS2_PLACEMENT_3D('',#15462,#12572,#12573);
#9998=AXIS2_PLACEMENT_3D('',#15463,#12574,#12575);
#9999=AXIS2_PLACEMENT_3D('',#15465,#12576,#12577);
#10000=AXIS2_PLACEMENT_3D('',#15468,#12579,#12580);
#10001=AXIS2_PLACEMENT_3D('',#15469,#12581,#12582);
#10002=AXIS2_PLACEMENT_3D('',#15470,#12583,#12584);
#12565=DIRECTION('axis',(0.,0.,1.));
#12566=DIRECTION('refdir',(1.,0.,0.));
#12567=DIRECTION('center_axis',(0.,1.,0.));
#12568=DIRECTION('ref_axis',(1.,0.,0.));
#12569=DIRECTION('center_axis',(0.,-1.,0.));
#12570=DIRECTION('ref_axis',(1.,0.,0.));
#12571=DIRECTION('',(0.,-1.,0.));
#12572=DIRECTION('center_axis',(0.,-1.,0.));
#12573=DIRECTION('ref_axis',(1.,0.,0.));
#12574=DIRECTION('center_axis',(0.,1.,0.));
#12575=DIRECTION('ref_axis',(1.,0.,0.));
#12576=DIRECTION('center_axis',(0.,1.,0.));
#12577=DIRECTION('ref_axis',(1.,0.,0.));
#12578=DIRECTION('',(0.,-1.,0.));
#12579=DIRECTION('center_axis',(0.,1.,0.));
#12580=DIRECTION('ref_axis',(1.,0.,0.));
#12581=DIRECTION('center_axis',(0.,1.,0.));
#12582=DIRECTION('ref_axis',(1.,0.,0.));
#12583=DIRECTION('center_axis',(0.,1.,0.));
#12584=DIRECTION('ref_axis',(1.,0.,0.));
#15456=CARTESIAN_POINT('',(0.,0.,0.));
#15457=CARTESIAN_POINT('Origin',(0.,14.35,3.5));
#15458=CARTESIAN_POINT('',(-1.1,14.55,3.5));
#15459=CARTESIAN_POINT('Origin',(0.,14.55,3.5));
#15460=CARTESIAN_POINT('',(-1.1,14.35,3.5));
#15461=CARTESIAN_POINT('',(-1.1,14.35,3.5));
#15462=CARTESIAN_POINT('Origin',(0.,14.35,3.5));
#15463=CARTESIAN_POINT('Origin',(0.,14.35,3.5));
#15464=CARTESIAN_POINT('',(-1.5,14.55,3.5));
#15465=CARTESIAN_POINT('Origin',(0.,14.55,3.5));
#15466=CARTESIAN_POINT('',(-1.5,14.35,3.5));
#15467=CARTESIAN_POINT('',(-1.5,14.35,3.5));
#15468=CARTESIAN_POINT('Origin',(0.,14.35,3.5));
#15469=CARTESIAN_POINT('Origin',(0.,14.55,3.5));
#15470=CARTESIAN_POINT('Origin',(0.,14.35,3.5));
#16200=UNCERTAINTY_MEASURE_WITH_UNIT(LENGTH_MEASURE(0.001),#16282,
'DISTANCE_ACCURACY_VALUE',
'Maximum model space distance between geometric entities at asserted c
onnectivities');
#16212=UNCERTAINTY_MEASURE_WITH_UNIT(LENGTH_MEASURE(0.001),#16282,
'DISTANCE_ACCURACY_VALUE',
'Maximum model space distance between geometric entities at asserted c
onnectivities');
#16269=(
GEOMETRIC_REPRESENTATION_CONTEXT(3)
GLOBAL_UNCERTAINTY_ASSIGNED_CONTEXT((#16200))
GLOBAL_UNIT_ASSIGNED_CONTEXT((#16282,#16284,#16285))
REPRESENTATION_CONTEXT('','3D')
);
#16281=(
GEOMETRIC_REPRESENTATION_CONTEXT(3)
GLOBAL_UNCERTAINTY_ASSIGNED_CONTEXT((#16212))
GLOBAL_UNIT_ASSIGNED_CONTEXT((#16282,#16284,#16285))
REPRESENTATION_CONTEXT('','3D')
);
#16282=(
LENGTH_UNIT()
NAMED_UNIT(*)
SI_UNIT(.CENTI.,.METRE.)
);
#16284=(
NAMED_UNIT(*)
PLANE_ANGLE_UNIT()
SI_UNIT($,.RADIAN.)
);
#16285=(
NAMED_UNIT(*)
SI_UNIT($,.STERADIAN.)
SOLID_ANGLE_UNIT()
);
#16342=SHAPE_DEFINITION_REPRESENTATION(#16476,#16575);
#16476=PRODUCT_DEFINITION_SHAPE('',$,#16644);
#16575=SHAPE_REPRESENTATION('',(#9994),#16269);
#16587=PRODUCT_DEFINITION_CONTEXT('part definition',#16793,'design');
#16644=PRODUCT_DEFINITION('Outer race retainer (4)',
'Outer race retainer (4)',#16712,#16587);
#16712=PRODUCT_DEFINITION_FORMATION('',$,#16851);
#16793=APPLICATION_CONTEXT(
'Core Data for Automotive Mechanical Design Process');
#16794=PRODUCT_CONTEXT('part definition',#16793,'mechanical');
#16851=PRODUCT('Outer race retainer (4)','Outer race retainer (4)',
'Outer race retainer (4)',(#16794));
#16926=COLOUR_RGB('Grey',0.48,0.52,0.57);
#16927=FILL_AREA_STYLE_COLOUR('',#16926);
#16928=FILL_AREA_STYLE('',(#16927));
#16929=SURFACE_STYLE_FILL_AREA(#16928);
#16930=SURFACE_SIDE_STYLE('',(#16929));
#16931=SURFACE_STYLE_USAGE(.BOTH.,#16930);
#16932=PRESENTATION_STYLE_ASSIGNMENT((#16931));
ENDSEC;
END-ISO-10303-21;
